ISO-10303-21;
HEADER;
/* Generated by software containing ST-Developer
 * from STEP Tools, Inc. (www.steptools.com) 
 */

FILE_DESCRIPTION(
/* description */ ('Pipe clamp stand with threaded column'),
/* implementation_level */ '2;1');

FILE_NAME(
/* name */ 'M6x18 mounting screw.step',
/* time_stamp */ '2026-10-27T10:55:48-07:00',
/* author */ (''),
/* organization */ (''),
/* preprocessor_version */ 'ST-DEVELOPER v20.2',
/* originating_system */ 'Autodesk Translation Framework v15.17.0.0',
/* authorisation */ '');

FILE_SCHEMA (('AUTOMOTIVE_DESIGN { 1 0 10303 214 3 1 1 }'));
ENDSEC;

DATA;
#10=MECHANICAL_DESIGN_GEOMETRIC_PRESENTATION_REPRESENTATION('',(#763),#34433);
#195=CONICAL_SURFACE('',#9522,0.475,0.785398163397449);
#196=CONICAL_SURFACE('',#9526,0.485,0.785398163397448);
#197=CONICAL_SURFACE('',#9530,0.31,0.463647609000806);
#203=ORIENTED_CLOSED_SHELL('',*,#8790,.F.);
#205=BREP_WITH_VOIDS('Body1',#8791,(#203));
#711=SHAPE_REPRESENTATION_RELATIONSHIP('SRR','None',#34553,#733);
#733=ADVANCED_BREP_SHAPE_REPRESENTATION('',(#205),#34421);
#763=STYLED_ITEM('',(#34750),#205);
#842=FACE_BOUND('',#1946,.T.);
#979=PLANE('',#9510);
#980=PLANE('',#9511);
#981=PLANE('',#9512);
#982=PLANE('',#9513);
#983=PLANE('',#9514);
#984=PLANE('',#9515);
#985=PLANE('',#9516);
#986=PLANE('',#9517);
#987=PLANE('',#9518);
#988=PLANE('',#9520);
#989=PLANE('',#9528);
#1402=FACE_OUTER_BOUND('',#1932,.T.);
#1403=FACE_OUTER_BOUND('',#1933,.T.);
#1404=FACE_OUTER_BOUND('',#1934,.T.);
#1405=FACE_OUTER_BOUND('',#1935,.T.);
#1406=FACE_OUTER_BOUND('',#1936,.T.);
#1407=FACE_OUTER_BOUND('',#1937,.T.);
#1408=FACE_OUTER_BOUND('',#1938,.T.);
#1409=FACE_OUTER_BOUND('',#1939,.T.);
#1410=FACE_OUTER_BOUND('',#1940,.T.);
#1411=FACE_OUTER_BOUND('',#1941,.T.);
#1412=FACE_OUTER_BOUND('',#1942,.T.);
#1413=FACE_OUTER_BOUND('',#1943,.T.);
#1414=FACE_OUTER_BOUND('',#1944,.T.);
#1415=FACE_OUTER_BOUND('',#1945,.T.);
#1416=FACE_OUTER_BOUND('',#1947,.T.);
#1417=FACE_OUTER_BOUND('',#1948,.T.);
#1932=EDGE_LOOP('',(#7379,#7380,#7381,#7382));
#1933=EDGE_LOOP('',(#7383,#7384,#7385,#7386));
#1934=EDGE_LOOP('',(#7387,#7388,#7389,#7390));
#1935=EDGE_LOOP('',(#7391,#7392,#7393,#7394));
#1936=EDGE_LOOP('',(#7395,#7396,#7397,#7398));
#1937=EDGE_LOOP('',(#7399,#7400,#7401,#7402));
#1938=EDGE_LOOP('',(#7403,#7404,#7405,#7406,#7407,#7408));
#1939=EDGE_LOOP('',(#7409,#7410,#7411,#7412,#7413,#7414));
#1940=EDGE_LOOP('',(#7415));
#1941=EDGE_LOOP('',(#7416));
#1942=EDGE_LOOP('',(#7417,#7418,#7419,#7420));
#1943=EDGE_LOOP('',(#7421,#7422,#7423,#7424));
#1944=EDGE_LOOP('',(#7425,#7426,#7427,#7428));
#1945=EDGE_LOOP('',(#7429));
#1946=EDGE_LOOP('',(#7430));
#1947=EDGE_LOOP('',(#7431,#7432,#7433,#7434));
#1948=EDGE_LOOP('',(#7435,#7436,#7437,#7438));
#2531=LINE('',#28682,#3148);
#2532=LINE('',#28684,#3149);
#2533=LINE('',#28686,#3150);
#2534=LINE('',#28687,#3151);
#2535=LINE('',#28690,#3152);
#2536=LINE('',#28692,#3153);
#2537=LINE('',#28693,#3154);
#2538=LINE('',#28696,#3155);
#2539=LINE('',#28698,#3156);
#2540=LINE('',#28699,#3157);
#2541=LINE('',#28702,#3158);
#2542=LINE('',#28704,#3159);
#2543=LINE('',#28705,#3160);
#2544=LINE('',#28708,#3161);
#2545=LINE('',#28710,#3162);
#2546=LINE('',#28711,#3163);
#2547=LINE('',#28713,#3164);
#2548=LINE('',#28714,#3165);
#2549=LINE('',#28726,#3166);
#2550=LINE('',#28730,#3167);
#2551=LINE('',#28734,#3168);
#2552=LINE('',#28741,#3169);
#2553=LINE('',#28743,#3170);
#3148=VECTOR('',#11116,1.);
#3149=VECTOR('',#11117,1.);
#3150=VECTOR('',#11118,1.);
#3151=VECTOR('',#11119,1.);
#3152=VECTOR('',#11122,1.);
#3153=VECTOR('',#11123,1.);
#3154=VECTOR('',#11124,1.);
#3155=VECTOR('',#11127,1.);
#3156=VECTOR('',#11128,1.);
#3157=VECTOR('',#11129,1.);
#3158=VECTOR('',#11132,1.);
#3159=VECTOR('',#11133,1.);
#3160=VECTOR('',#11134,1.);
#3161=VECTOR('',#11137,1.);
#3162=VECTOR('',#11138,1.);
#3163=VECTOR('',#11139,1.);
#3164=VECTOR('',#11142,1.);
#3165=VECTOR('',#11143,1.);
#3166=VECTOR('',#11160,0.475);
#3167=VECTOR('',#11165,0.5);
#3168=VECTOR('',#11170,0.485);
#3169=VECTOR('',#11179,0.31);
#3170=VECTOR('',#11182,0.3);
#3404=CIRCLE('',#9519,0.2942);
#3405=CIRCLE('',#9521,0.45);
#3406=CIRCLE('',#9523,0.5);
#3407=CIRCLE('',#9525,0.5);
#3408=CIRCLE('',#9527,0.47);
#3409=CIRCLE('',#9529,0.32);
#3410=CIRCLE('',#9531,0.2942);
#4066=VERTEX_POINT('',#28680);
#4067=VERTEX_POINT('',#28681);
#4068=VERTEX_POINT('',#28683);
#4069=VERTEX_POINT('',#28685);
#4070=VERTEX_POINT('',#28689);
#4071=VERTEX_POINT('',#28691);
#4072=VERTEX_POINT('',#28695);
#4073=VERTEX_POINT('',#28697);
#4074=VERTEX_POINT('',#28701);
#4075=VERTEX_POINT('',#28703);
#4076=VERTEX_POINT('',#28707);
#4077=VERTEX_POINT('',#28709);
#4078=VERTEX_POINT('',#28718);
#4079=VERTEX_POINT('',#28721);
#4080=VERTEX_POINT('',#28724);
#4081=VERTEX_POINT('',#28728);
#4082=VERTEX_POINT('',#28732);
#4083=VERTEX_POINT('',#28736);
#4084=VERTEX_POINT('',#28739);
#5203=EDGE_CURVE('',#4066,#4067,#2531,.T.);
#5204=EDGE_CURVE('',#4067,#4068,#2532,.T.);
#5205=EDGE_CURVE('',#4068,#4069,#2533,.T.);
#5206=EDGE_CURVE('',#4066,#4069,#2534,.T.);
#5207=EDGE_CURVE('',#4067,#4070,#2535,.T.);
#5208=EDGE_CURVE('',#4070,#4071,#2536,.T.);
#5209=EDGE_CURVE('',#4071,#4068,#2537,.T.);
#5210=EDGE_CURVE('',#4070,#4072,#2538,.T.);
#5211=EDGE_CURVE('',#4072,#4073,#2539,.T.);
#5212=EDGE_CURVE('',#4073,#4071,#2540,.T.);
#5213=EDGE_CURVE('',#4072,#4074,#2541,.T.);
#5214=EDGE_CURVE('',#4074,#4075,#2542,.T.);
#5215=EDGE_CURVE('',#4075,#4073,#2543,.T.);
#5216=EDGE_CURVE('',#4074,#4076,#2544,.T.);
#5217=EDGE_CURVE('',#4076,#4077,#2545,.T.);
#5218=EDGE_CURVE('',#4077,#4075,#2546,.T.);
#5219=EDGE_CURVE('',#4076,#4066,#2547,.T.);
#5220=EDGE_CURVE('',#4069,#4077,#2548,.T.);
#5221=EDGE_CURVE('',#4078,#4078,#3404,.T.);
#5222=EDGE_CURVE('',#4079,#4079,#3405,.T.);
#5223=EDGE_CURVE('',#4080,#4080,#3406,.T.);
#5224=EDGE_CURVE('',#4080,#4079,#2549,.T.);
#5225=EDGE_CURVE('',#4081,#4081,#3407,.T.);
#5226=EDGE_CURVE('',#4081,#4080,#2550,.T.);
#5227=EDGE_CURVE('',#4082,#4082,#3408,.T.);
#5228=EDGE_CURVE('',#4082,#4081,#2551,.T.);
#5229=EDGE_CURVE('',#4083,#4083,#3409,.T.);
#5230=EDGE_CURVE('',#4084,#4084,#3410,.F.);
#5231=EDGE_CURVE('',#4084,#4083,#2552,.T.);
#5232=EDGE_CURVE('',#4078,#4084,#2553,.T.);
#7379=ORIENTED_EDGE('',*,*,#5203,.T.);
#7380=ORIENTED_EDGE('',*,*,#5204,.T.);
#7381=ORIENTED_EDGE('',*,*,#5205,.T.);
#7382=ORIENTED_EDGE('',*,*,#5206,.F.);
#7383=ORIENTED_EDGE('',*,*,#5207,.T.);
#7384=ORIENTED_EDGE('',*,*,#5208,.T.);
#7385=ORIENTED_EDGE('',*,*,#5209,.T.);
#7386=ORIENTED_EDGE('',*,*,#5204,.F.);
#7387=ORIENTED_EDGE('',*,*,#5210,.T.);
#7388=ORIENTED_EDGE('',*,*,#5211,.T.);
#7389=ORIENTED_EDGE('',*,*,#5212,.T.);
#7390=ORIENTED_EDGE('',*,*,#5208,.F.);
#7391=ORIENTED_EDGE('',*,*,#5213,.T.);
#7392=ORIENTED_EDGE('',*,*,#5214,.T.);
#7393=ORIENTED_EDGE('',*,*,#5215,.T.);
#7394=ORIENTED_EDGE('',*,*,#5211,.F.);
#7395=ORIENTED_EDGE('',*,*,#5216,.T.);
#7396=ORIENTED_EDGE('',*,*,#5217,.T.);
#7397=ORIENTED_EDGE('',*,*,#5218,.T.);
#7398=ORIENTED_EDGE('',*,*,#5214,.F.);
#7399=ORIENTED_EDGE('',*,*,#5219,.T.);
#7400=ORIENTED_EDGE('',*,*,#5206,.T.);
#7401=ORIENTED_EDGE('',*,*,#5220,.T.);
#7402=ORIENTED_EDGE('',*,*,#5217,.F.);
#7403=ORIENTED_EDGE('',*,*,#5219,.F.);
#7404=ORIENTED_EDGE('',*,*,#5216,.F.);
#7405=ORIENTED_EDGE('',*,*,#5213,.F.);
#7406=ORIENTED_EDGE('',*,*,#5210,.F.);
#7407=ORIENTED_EDGE('',*,*,#5207,.F.);
#7408=ORIENTED_EDGE('',*,*,#5203,.F.);
#7409=ORIENTED_EDGE('',*,*,#5220,.F.);
#7410=ORIENTED_EDGE('',*,*,#5205,.F.);
#7411=ORIENTED_EDGE('',*,*,#5209,.F.);
#7412=ORIENTED_EDGE('',*,*,#5212,.F.);
#7413=ORIENTED_EDGE('',*,*,#5215,.F.);
#7414=ORIENTED_EDGE('',*,*,#5218,.F.);
#7415=ORIENTED_EDGE('',*,*,#5221,.F.);
#7416=ORIENTED_EDGE('',*,*,#5222,.F.);
#7417=ORIENTED_EDGE('',*,*,#5223,.F.);
#7418=ORIENTED_EDGE('',*,*,#5224,.T.);
#7419=ORIENTED_EDGE('',*,*,#5222,.T.);
#7420=ORIENTED_EDGE('',*,*,#5224,.F.);
#7421=ORIENTED_EDGE('',*,*,#5225,.F.);
#7422=ORIENTED_EDGE('',*,*,#5226,.T.);
#7423=ORIENTED_EDGE('',*,*,#5223,.T.);
#7424=ORIENTED_EDGE('',*,*,#5226,.F.);
#7425=ORIENTED_EDGE('',*,*,#5227,.F.);
#7426=ORIENTED_EDGE('',*,*,#5228,.T.);
#7427=ORIENTED_EDGE('',*,*,#5225,.T.);
#7428=ORIENTED_EDGE('',*,*,#5228,.F.);
#7429=ORIENTED_EDGE('',*,*,#5227,.T.);
#7430=ORIENTED_EDGE('',*,*,#5229,.F.);
#7431=ORIENTED_EDGE('',*,*,#5230,.F.);
#7432=ORIENTED_EDGE('',*,*,#5231,.T.);
#7433=ORIENTED_EDGE('',*,*,#5229,.T.);
#7434=ORIENTED_EDGE('',*,*,#5231,.F.);
#7435=ORIENTED_EDGE('',*,*,#5221,.T.);
#7436=ORIENTED_EDGE('',*,*,#5232,.T.);
#7437=ORIENTED_EDGE('',*,*,#5230,.T.);
#7438=ORIENTED_EDGE('',*,*,#5232,.F.);
#8233=CYLINDRICAL_SURFACE('',#9524,0.5);
#8234=CYLINDRICAL_SURFACE('',#9532,0.2942);
#8639=ADVANCED_FACE('',(#1402),#979,.F.);
#8640=ADVANCED_FACE('',(#1403),#980,.F.);
#8641=ADVANCED_FACE('',(#1404),#981,.F.);
#8642=ADVANCED_FACE('',(#1405),#982,.F.);
#8643=ADVANCED_FACE('',(#1406),#983,.F.);
#8644=ADVANCED_FACE('',(#1407),#984,.F.);
#8645=ADVANCED_FACE('',(#1408),#985,.F.);
#8646=ADVANCED_FACE('',(#1409),#986,.F.);
#8647=ADVANCED_FACE('',(#1410),#987,.F.);
#8648=ADVANCED_FACE('',(#1411),#988,.T.);
#8649=ADVANCED_FACE('',(#1412),#195,.T.);
#8650=ADVANCED_FACE('',(#1413),#8233,.T.);
#8651=ADVANCED_FACE('',(#1414),#196,.T.);
#8652=ADVANCED_FACE('',(#1415,#842),#989,.T.);
#8653=ADVANCED_FACE('',(#1416),#197,.T.);
#8654=ADVANCED_FACE('',(#1417),#8234,.T.);
#8790=CLOSED_SHELL('',(#8639,#8640,#8641,#8642,#8643,#8644,#8645,#8646));
#8791=CLOSED_SHELL('',(#8647,#8648,#8649,#8650,#8651,#8652,#8653,#8654));
#9509=AXIS2_PLACEMENT_3D('',#28678,#11112,#11113);
#9510=AXIS2_PLACEMENT_3D('',#28679,#11114,#11115);
#9511=AXIS2_PLACEMENT_3D('',#28688,#11120,#11121);
#9512=AXIS2_PLACEMENT_3D('',#28694,#11125,#11126);
#9513=AXIS2_PLACEMENT_3D('',#28700,#11130,#11131);
#9514=AXIS2_PLACEMENT_3D('',#28706,#11135,#11136);
#9515=AXIS2_PLACEMENT_3D('',#28712,#11140,#11141);
#9516=AXIS2_PLACEMENT_3D('',#28715,#11144,#11145);
#9517=AXIS2_PLACEMENT_3D('',#28716,#11146,#11147);
#9518=AXIS2_PLACEMENT_3D('',#28717,#11148,#11149);
#9519=AXIS2_PLACEMENT_3D('',#28719,#11150,#11151);
#9520=AXIS2_PLACEMENT_3D('',#28720,#11152,#11153);
#9521=AXIS2_PLACEMENT_3D('',#28722,#11154,#11155);
#9522=AXIS2_PLACEMENT_3D('',#28723,#11156,#11157);
#9523=AXIS2_PLACEMENT_3D('',#28725,#11158,#11159);
#9524=AXIS2_PLACEMENT_3D('',#28727,#11161,#11162);
#9525=AXIS2_PLACEMENT_3D('',#28729,#11163,#11164);
#9526=AXIS2_PLACEMENT_3D('',#28731,#11166,#11167);
#9527=AXIS2_PLACEMENT_3D('',#28733,#11168,#11169);
#9528=AXIS2_PLACEMENT_3D('',#28735,#11171,#11172);
#9529=AXIS2_PLACEMENT_3D('',#28737,#11173,#11174);
#9530=AXIS2_PLACEMENT_3D('',#28738,#11175,#11176);
#9531=AXIS2_PLACEMENT_3D('',#28740,#11177,#11178);
#9532=AXIS2_PLACEMENT_3D('',#28742,#11180,#11181);
#11112=DIRECTION('axis',(0.,0.,1.));
#11113=DIRECTION('refdir',(1.,0.,0.));
#11114=DIRECTION('center_axis',(0.866025403784439,0.,-0.5));
#11115=DIRECTION('ref_axis',(0.5,0.,0.866025403784439));
#11116=DIRECTION('',(-0.5,0.,-0.866025403784439));
#11117=DIRECTION('',(0.,-1.,0.));
#11118=DIRECTION('',(0.5,0.,0.866025403784439));
#11119=DIRECTION('',(0.,-1.,0.));
#11120=DIRECTION('center_axis',(1.92296268638356E-16,0.,-1.));
#11121=DIRECTION('ref_axis',(1.,0.,1.92296268638356E-16));
#11122=DIRECTION('',(-1.,0.,-1.92296268638356E-16));
#11123=DIRECTION('',(0.,-1.,0.));
#11124=DIRECTION('',(1.,0.,1.92296268638356E-16));
#11125=DIRECTION('center_axis',(-0.866025403784439,0.,-0.5));
#11126=DIRECTION('ref_axis',(0.5,0.,-0.866025403784439));
#11127=DIRECTION('',(-0.5,0.,0.866025403784438));
#11128=DIRECTION('',(0.,-1.,0.));
#11129=DIRECTION('',(0.5,0.,-0.866025403784438));
#11130=DIRECTION('center_axis',(-0.866025403784439,0.,0.5));
#11131=DIRECTION('ref_axis',(-0.5,0.,-0.866025403784439));
#11132=DIRECTION('',(0.5,0.,0.866025403784439));
#11133=DIRECTION('',(0.,-1.,0.));
#11134=DIRECTION('',(-0.5,0.,-0.866025403784439));
#11135=DIRECTION('center_axis',(-1.92296268638356E-16,0.,1.));
#11136=DIRECTION('ref_axis',(-1.,0.,-1.92296268638356E-16));
#11137=DIRECTION('',(1.,0.,1.92296268638356E-16));
#11138=DIRECTION('',(0.,-1.,0.));
#11139=DIRECTION('',(-1.,0.,-1.92296268638356E-16));
#11140=DIRECTION('center_axis',(0.866025403784439,0.,0.5));
#11141=DIRECTION('ref_axis',(-0.5,0.,0.866025403784439));
#11142=DIRECTION('',(0.5,0.,-0.866025403784439));
#11143=DIRECTION('',(-0.5,0.,0.866025403784439));
#11144=DIRECTION('center_axis',(0.,1.,0.));
#11145=DIRECTION('ref_axis',(1.,0.,0.));
#11146=DIRECTION('center_axis',(0.,-1.,0.));
#11147=DIRECTION('ref_axis',(0.,0.,-1.));
#11148=DIRECTION('center_axis',(0.,1.,0.));
#11149=DIRECTION('ref_axis',(1.,0.,0.));
#11150=DIRECTION('center_axis',(0.,1.,0.));
#11151=DIRECTION('ref_axis',(1.,0.,0.));
#11152=DIRECTION('center_axis',(0.,1.,0.));
#11153=DIRECTION('ref_axis',(0.,0.,1.));
#11154=DIRECTION('center_axis',(0.,-1.,0.));
#11155=DIRECTION('ref_axis',(1.,0.,0.));
#11156=DIRECTION('center_axis',(0.,-1.,0.));
#11157=DIRECTION('ref_axis',(1.,0.,0.));
#11158=DIRECTION('center_axis',(0.,-1.,0.));
#11159=DIRECTION('ref_axis',(1.,0.,0.));
#11160=DIRECTION('',(0.707106781186548,0.707106781186547,8.65956056235494E-17));
#11161=DIRECTION('center_axis',(0.,-1.,0.));
#11162=DIRECTION('ref_axis',(1.,0.,0.));
#11163=DIRECTION('center_axis',(0.,-1.,0.));
#11164=DIRECTION('ref_axis',(1.,0.,0.));
#11165=DIRECTION('',(0.,1.,0.));
#11166=DIRECTION('center_axis',(0.,1.,0.));
#11167=DIRECTION('ref_axis',(1.,0.,0.));
#11168=DIRECTION('center_axis',(0.,-1.,0.));
#11169=DIRECTION('ref_axis',(1.,0.,0.));
#11170=DIRECTION('',(-0.707106781186547,0.707106781186548,-8.65956056235493E-17));
#11171=DIRECTION('center_axis',(0.,-1.,0.));
#11172=DIRECTION('ref_axis',(0.,0.,-1.));
#11173=DIRECTION('center_axis',(0.,-1.,0.));
#11174=DIRECTION('ref_axis',(1.,0.,0.));
#11175=DIRECTION('center_axis',(0.,1.,0.));
#11176=DIRECTION('ref_axis',(1.,0.,0.));
#11177=DIRECTION('center_axis',(0.,1.,0.));
#11178=DIRECTION('ref_axis',(1.,0.,0.));
#11179=DIRECTION('',(-0.447213595499958,0.894427190999916,-5.47678698264203E-17));
#11180=DIRECTION('center_axis',(0.,-1.,0.));
#11181=DIRECTION('ref_axis',(1.,0.,0.));
#11182=DIRECTION('',(0.,1.,0.));
#28678=CARTESIAN_POINT('',(0.,0.,0.));
#28679=CARTESIAN_POINT('Origin',(0.144337567297406,-0.6,-0.25));
#28680=CARTESIAN_POINT('',(0.288675134594813,-0.6,0.));
#28681=CARTESIAN_POINT('',(0.144337567297406,-0.6,-0.25));
#28682=CARTESIAN_POINT('',(0.288675134594813,-0.6,0.));
#28683=CARTESIAN_POINT('',(0.144337567297406,-0.96,-0.25));
#28684=CARTESIAN_POINT('',(0.144337567297406,-0.6,-0.25));
#28685=CARTESIAN_POINT('',(0.288675134594813,-0.96,0.));
#28686=CARTESIAN_POINT('',(0.288675134594813,-0.96,0.));
#28687=CARTESIAN_POINT('',(0.288675134594813,-0.6,0.));
#28688=CARTESIAN_POINT('Origin',(-0.144337567297406,-0.6,-0.25));
#28689=CARTESIAN_POINT('',(-0.144337567297406,-0.6,-0.25));
#28690=CARTESIAN_POINT('',(0.144337567297406,-0.6,-0.25));
#28691=CARTESIAN_POINT('',(-0.144337567297406,-0.96,-0.25));
#28692=CARTESIAN_POINT('',(-0.144337567297406,-0.6,-0.25));
#28693=CARTESIAN_POINT('',(0.144337567297406,-0.96,-0.25));
#28694=CARTESIAN_POINT('Origin',(-0.288675134594813,-0.6,-8.32667268468867E-17));
#28695=CARTESIAN_POINT('',(-0.288675134594813,-0.6,-3.53525079574969E-17));
#28696=CARTESIAN_POINT('',(-0.144337567297406,-0.6,-0.25));
#28697=CARTESIAN_POINT('',(-0.288675134594813,-0.96,-5.55111512312578E-17));
#28698=CARTESIAN_POINT('',(-0.288675134594813,-0.6,-3.53525079574969E-17));
#28699=CARTESIAN_POINT('',(-0.144337567297406,-0.96,-0.25));
#28700=CARTESIAN_POINT('Origin',(-0.144337567297407,-0.6,0.25));
#28701=CARTESIAN_POINT('',(-0.144337567297407,-0.6,0.25));
#28702=CARTESIAN_POINT('',(-0.288675134594813,-0.6,-3.53525079574969E-17));
#28703=CARTESIAN_POINT('',(-0.144337567297407,-0.96,0.25));
#28704=CARTESIAN_POINT('',(-0.144337567297407,-0.6,0.25));
#28705=CARTESIAN_POINT('',(-0.288675134594813,-0.96,-3.53525079574969E-17));
#28706=CARTESIAN_POINT('Origin',(0.144337567297406,-0.6,0.25));
#28707=CARTESIAN_POINT('',(0.144337567297406,-0.6,0.25));
#28708=CARTESIAN_POINT('',(-0.144337567297407,-0.6,0.25));
#28709=CARTESIAN_POINT('',(0.144337567297406,-0.96,0.25));
#28710=CARTESIAN_POINT('',(0.144337567297406,-0.6,0.25));
#28711=CARTESIAN_POINT('',(-0.144337567297407,-0.96,0.25));
#28712=CARTESIAN_POINT('Origin',(0.288675134594813,-0.6,0.));
#28713=CARTESIAN_POINT('',(0.144337567297406,-0.6,0.25));
#28714=CARTESIAN_POINT('',(0.144337567297406,-0.96,0.25));
#28715=CARTESIAN_POINT('Origin',(0.,-0.6,0.));
#28716=CARTESIAN_POINT('Origin',(0.,-0.96,0.));
#28717=CARTESIAN_POINT('Origin',(0.,-1.8,0.));
#28718=CARTESIAN_POINT('',(-0.2942,-1.8,3.60291088309151E-17));
#28719=CARTESIAN_POINT('Origin',(0.,-1.8,0.));
#28720=CARTESIAN_POINT('Origin',(0.45,0.6,0.));
#28721=CARTESIAN_POINT('',(-0.45,0.6,-5.51091059616309E-17));
#28722=CARTESIAN_POINT('Origin',(0.,0.6,0.));
#28723=CARTESIAN_POINT('Origin',(0.,0.575,0.));
#28724=CARTESIAN_POINT('',(-0.5,0.55,-6.12323399573677E-17));
#28725=CARTESIAN_POINT('Origin',(0.,0.55,0.));
#28726=CARTESIAN_POINT('',(-0.475,0.575,-5.81707229594993E-17));
#28727=CARTESIAN_POINT('Origin',(0.,0.29,0.));
#28728=CARTESIAN_POINT('',(-0.5,0.0299999999999998,-6.12323399573677E-17));
#28729=CARTESIAN_POINT('Origin',(0.,0.0299999999999998,0.));
#28730=CARTESIAN_POINT('',(-0.5,0.29,-6.12323399573677E-17));
#28731=CARTESIAN_POINT('Origin',(0.,0.0150000000000001,0.));
#28732=CARTESIAN_POINT('',(-0.47,7.11236625150491E-17,-5.75583995599256E-17));
#28733=CARTESIAN_POINT('Origin',(0.,0.,0.));
#28734=CARTESIAN_POINT('',(-0.485,0.0150000000000001,-5.93953697586466E-17));
#28735=CARTESIAN_POINT('Origin',(0.32,0.,0.));
#28736=CARTESIAN_POINT('',(-0.32,-6.93889390390723E-18,-3.91886975727153E-17));
#28737=CARTESIAN_POINT('Origin',(0.,0.,0.));
#28738=CARTESIAN_POINT('Origin',(0.,-0.02,0.));
#28739=CARTESIAN_POINT('',(-0.2942,-0.0515999999999999,3.60291088309151E-17));
#28740=CARTESIAN_POINT('Origin',(0.,-0.0515999999999999,0.));
#28741=CARTESIAN_POINT('',(-0.31,-0.02,-3.7964050773568E-17));
#28742=CARTESIAN_POINT('Origin',(0.,-1.24,0.));
#28743=CARTESIAN_POINT('',(-0.2942,-1.24,-3.60291088309151E-17));
#34392=UNCERTAINTY_MEASURE_WITH_UNIT(LENGTH_MEASURE(0.001),#34434,
'DISTANCE_ACCURACY_VALUE',
'Maximum model space distance between geometric entities at asserted c
onnectivities');
#34404=UNCERTAINTY_MEASURE_WITH_UNIT(LENGTH_MEASURE(0.001),#34434,
'DISTANCE_ACCURACY_VALUE',
'Maximum model space distance between geometric entities at asserted c
onnectivities');
#34421=(
GEOMETRIC_REPRESENTATION_CONTEXT(3)
GLOBAL_UNCERTAINTY_ASSIGNED_CONTEXT((#34392))
GLOBAL_UNIT_ASSIGNED_CONTEXT((#34434,#34436,#34437))
REPRESENTATION_CONTEXT('','3D')
);
#34433=(
GEOMETRIC_REPRESENTATION_CONTEXT(3)
GLOBAL_UNCERTAINTY_ASSIGNED_CONTEXT((#34404))
GLOBAL_UNIT_ASSIGNED_CONTEXT((#34434,#34436,#34437))
REPRESENTATION_CONTEXT('','3D')
);
#34434=(
LENGTH_UNIT()
NAMED_UNIT(*)
SI_UNIT(.CENTI.,.METRE.)
);
#34436=(
NAMED_UNIT(*)
PLANE_ANGLE_UNIT()
SI_UNIT($,.RADIAN.)
);
#34437=(
NAMED_UNIT(*)
SI_UNIT($,.STERADIAN.)
SOLID_ANGLE_UNIT()
);
#34454=SHAPE_DEFINITION_REPRESENTATION(#34482,#34553);
#34482=PRODUCT_DEFINITION_SHAPE('',$,#34582);
#34553=SHAPE_REPRESENTATION('',(#9509),#34421);
#34565=PRODUCT_DEFINITION_CONTEXT('part definition',#34651,'design');
#34582=PRODUCT_DEFINITION('M6x18 mounting screw','M6x18 mounting screw',
#34610,#34565);
#34610=PRODUCT_DEFINITION_FORMATION('',$,#34669);
#34651=APPLICATION_CONTEXT(
'Core Data for Automotive Mechanical Design Process');
#34652=PRODUCT_CONTEXT('part definition',#34651,'mechanical');
#34669=PRODUCT('M6x18 mounting screw','M6x18 mounting screw',
'M6x18 mounting screw',(#34652));
#34744=COLOUR_RGB('Black',0.12,0.14,0.17);
#34745=FILL_AREA_STYLE_COLOUR('',#34744);
#34746=FILL_AREA_STYLE('',(#34745));
#34747=SURFACE_STYLE_FILL_AREA(#34746);
#34748=SURFACE_SIDE_STYLE('',(#34747));
#34749=SURFACE_STYLE_USAGE(.BOTH.,#34748);
#34750=PRESENTATION_STYLE_ASSIGNMENT((#34749));
ENDSEC;
END-ISO-10303-21;
